ISO-10303-21;
HEADER;
FILE_DESCRIPTION (('STEP AP214'),
    '1' );
FILE_NAME ('Part15.step',
    '2026-11-01T06:29:40',
    ( '' ),
    ( '' ),
    'SwSTEP 2.0',
    'SolidWorks 2024',
    '' );
FILE_SCHEMA (( 'AUTOMOTIVE_DESIGN' ));
ENDSEC;

DATA;
#55=LINE ( 'NONE', #6674, #3407 ) ;
#114=COLOUR_RGB ( '', 0.72549020, 0.75294118, 0.79215686) ;
#135=DIRECTION ( 'NONE',  ( -1.000000000000000000, -0.000000000000000000, -0.000000000000000000 ) ) ;
#157=FACE_OUTER_BOUND ( 'NONE', #9168, .T. ) ;
#229=SURFACE_STYLE_USAGE ( .BOTH. , #1757 ) ;
#249=AXIS2_PLACEMENT_3D ( 'NONE', #16527, #16428, #14757 ) ;
#272=PLANE ( 'NONE',  #1506 ) ;
#294=EDGE_CURVE ( 'NONE', #16045, #3349, #13619, .T. ) ;
#371=CARTESIAN_POINT ( 'NONE',  ( 40.00000000000001421, 0.000000000000000000, -150.0000000000000000 ) ) ;
#489=DIRECTION ( 'NONE',  ( 0.000000000000000000, 1.000000000000000000, 0.000000000000000000 ) ) ;
#500=ORIENTED_EDGE ( 'NONE', *, *, #7079, .F. ) ;
#655=EDGE_CURVE ( 'NONE', #3196, #7067, #16936, .T. ) ;
#830=ORIENTED_EDGE ( 'NONE', *, *, #15569, .T. ) ;
#902=DIRECTION ( 'NONE',  ( -0.000000000000000000, -0.000000000000000000, 1.000000000000000000 ) ) ;
#965=DIRECTION ( 'NONE',  ( -1.000000000000000000, -0.000000000000000000, 0.000000000000000000 ) ) ;
#1033=AXIS2_PLACEMENT_3D ( 'NONE', #6804, #489, #6898 ) ;
#1057=AXIS2_PLACEMENT_3D ( 'NONE', #6619, #7198, #5069 ) ;
#1072=DIRECTION ( 'NONE',  ( -1.000000000000000000, -0.000000000000000000, -0.000000000000000000 ) ) ;
#1103=AXIS2_PLACEMENT_3D ( 'NONE', #2099, #16261, #10058 ) ;
#1129=PRODUCT_DEFINITION ( 'UNKNOWN', '', #19816, #15036 ) ;
#1289=AXIS2_PLACEMENT_3D ( 'NONE', #6135, #18680, #18875 ) ;
#1331=CYLINDRICAL_SURFACE ( 'NONE', #7752, 4.999999999999997335 ) ;
#1347=CYLINDRICAL_SURFACE ( 'NONE', #4460, 3.000000000000000888 ) ;
#1358=EDGE_CURVE ( 'NONE', #3349, #20011, #6222, .T. ) ;
#1382=DIRECTION ( 'NONE',  ( 0.000000000000000000, 0.000000000000000000, 1.000000000000000000 ) ) ;
#1419=CARTESIAN_POINT ( 'NONE',  ( 40.00000000000001421, 0.000000000000000000, -150.0000000000000000 ) ) ;
#1423=( GEOMETRIC_REPRESENTATION_CONTEXT ( 3 ) GLOBAL_UNCERTAINTY_ASSIGNED_CONTEXT ( ( #13454 ) ) GLOBAL_UNIT_ASSIGNED_CONTEXT ( ( #11249, #2063, #8380 ) ) REPRESENTATION_CONTEXT ( 'NONE', 'WORKASPACE' ) );
#1429=DIRECTION ( 'NONE',  ( 1.000000000000000000, 0.000000000000000000, -0.000000000000000000 ) ) ;
#1489=MANIFOLD_SOLID_BREP ( 'Cut-Extrude1', #6378 ) ;
#1506=AXIS2_PLACEMENT_3D ( 'NONE', #3487, #9769, #16078 ) ;
#1628=LINE ( 'NONE', #12486, #13295 ) ;
#1646=LINE ( 'NONE', #14245, #13340 ) ;
#1651=FACE_OUTER_BOUND ( 'NONE', #17246, .T. ) ;
#1704=ORIENTED_EDGE ( 'NONE', *, *, #13297, .F. ) ;
#1757=SURFACE_SIDE_STYLE ('',( #12923 ) ) ;
#1780=EDGE_CURVE ( 'NONE', #3349, #4170, #15304, .T. ) ;
#1798=CYLINDRICAL_SURFACE ( 'NONE', #1103, 3.000000000000002665 ) ;
#1830=DIRECTION ( 'NONE',  ( -0.000000000000000000, -0.000000000000000000, 1.000000000000000000 ) ) ;
#1975=ORIENTED_EDGE ( 'NONE', *, *, #11903, .T. ) ;
#2003=ORIENTED_EDGE ( 'NONE', *, *, #13776, .T. ) ;
#2018=ORIENTED_EDGE ( 'NONE', *, *, #16709, .T. ) ;
#2063=( NAMED_UNIT ( * ) PLANE_ANGLE_UNIT ( ) SI_UNIT ( $, .RADIAN. ) );
#2099=CARTESIAN_POINT ( 'NONE',  ( 40.00000000000001421, 0.000000000000000000, -150.0000000000000000 ) ) ;
#2150=CARTESIAN_POINT ( 'NONE',  ( 40.00000000000001421, 0.000000000000000000, 0.000000000000000000 ) ) ;
#2205=( NAMED_UNIT ( * ) PLANE_ANGLE_UNIT ( ) SI_UNIT ( $, .RADIAN. ) );
#2223=EDGE_CURVE ( 'NONE', #10797, #3197, #16228, .T. ) ;
#2304=( NAMED_UNIT ( * ) SI_UNIT ( $, .STERADIAN. ) SOLID_ANGLE_UNIT ( ) );
#2380=DIRECTION ( 'NONE',  ( 1.000000000000000000, 0.000000000000000000, 0.000000000000000000 ) ) ;
#2431=CARTESIAN_POINT ( 'NONE',  ( 0.000000000000000000, 5.000000000000000888, 0.000000000000000000 ) ) ;
#2471=DIRECTION ( 'NONE',  ( 1.000000000000000000, 0.000000000000000000, 0.000000000000000000 ) ) ;
#2543=CARTESIAN_POINT ( 'NONE',  ( 0.000000000000000000, 5.000000000000000888, 0.000000000000000000 ) ) ;
#2639=CARTESIAN_POINT ( 'NONE',  ( 0.000000000000000000, 5.000000000000000888, -150.0000000000000000 ) ) ;
#2691=AXIS2_PLACEMENT_3D ( 'NONE', #4919, #1382, #12764 ) ;
#2697=CIRCLE ( 'NONE', #16243, 3.000000000000002665 ) ;
#2712=LINE ( 'NONE', #12415, #8057 ) ;
#2726=ORIENTED_EDGE ( 'NONE', *, *, #18467, .F. ) ;
#2728=EDGE_LOOP ( 'NONE', ( #17079, #11265, #11947, #5482 ) ) ;
#2734=LINE ( 'NONE', #18490, #3378 ) ;
#2741=AXIS2_PLACEMENT_3D ( 'NONE', #5042, #3500, #8234 ) ;
#2748=LINE ( 'NONE', #2543, #16157 ) ;
#2797=CARTESIAN_POINT ( 'NONE',  ( 0.000000000000000000, 0.000000000000000000, -150.0000000000000000 ) ) ;
#2813=FACE_OUTER_BOUND ( 'NONE', #16072, .T. ) ;
#2953=CARTESIAN_POINT ( 'NONE',  ( 43.00000000000001421, 0.000000000000000000, 0.000000000000000000 ) ) ;
#2965=DIRECTION ( 'NONE',  ( 1.000000000000000000, 0.000000000000000000, 0.000000000000000000 ) ) ;
#3073=ADVANCED_FACE ( 'NONE', ( #12876 ), #11423, .F. ) ;
#3136=EDGE_LOOP ( 'NONE', ( #10951, #16764, #3766, #2003 ) ) ;
#3196=VERTEX_POINT ( 'NONE', #2431 ) ;
#3197=VERTEX_POINT ( 'NONE', #8737 ) ;
#3250=LINE ( 'NONE', #6457, #13197 ) ;
#3349=VERTEX_POINT ( 'NONE', #17156 ) ;
#3352=DIRECTION ( 'NONE',  ( 1.000000000000000000, 0.000000000000000000, 0.000000000000000000 ) ) ;
#3378=VECTOR ( 'NONE', #18387, 1000.000000000000000 ) ;
#3407=VECTOR ( 'NONE', #12755, 1000.000000000000000 ) ;
#3425=STYLED_ITEM ( 'NONE', ( #5194 ), #1489 ) ;
#3487=CARTESIAN_POINT ( 'NONE',  ( 0.000000000000000000, -3.000000000000000888, -150.0000000000000000 ) ) ;
#3491=DIRECTION ( 'NONE',  ( 1.000000000000000000, 0.000000000000000000, 0.000000000000000000 ) ) ;
#3500=DIRECTION ( 'NONE',  ( 0.000000000000000000, 0.000000000000000000, 1.000000000000000000 ) ) ;
#3509=CARTESIAN_POINT ( 'NONE',  ( 40.00000000000001421, 0.000000000000000000, -150.0000000000000000 ) ) ;
#3510=EDGE_LOOP ( 'NONE', ( #6417, #9656, #7137, #11391, #18853 ) ) ;
#3734=LINE ( 'NONE', #6840, #16497 ) ;
#3766=ORIENTED_EDGE ( 'NONE', *, *, #17198, .F. ) ;
#3819=CARTESIAN_POINT ( 'NONE',  ( 0.000000000000000000, -5.000000000000000888, 0.000000000000000000 ) ) ;
#3877=SHAPE_REPRESENTATION_RELATIONSHIP ( 'NONE' , 'NONE' ,  #13798, #13320 ) ;
#3918=AXIS2_PLACEMENT_3D ( 'NONE', #2797, #9097, #16190 ) ;
#3963=AXIS2_PLACEMENT_3D ( 'NONE', #2150, #14939, #16404 ) ;
#4029=EDGE_LOOP ( 'NONE', ( #12026, #18408, #16100, #6933 ) ) ;
#4170=VERTEX_POINT ( 'NONE', #8023 ) ;
#4243=LINE ( 'NONE', #8295, #8764 ) ;
#4433=ORIENTED_EDGE ( 'NONE', *, *, #1358, .F. ) ;
#4460=AXIS2_PLACEMENT_3D ( 'NONE', #7679, #19715, #5628 ) ;
#4485=LINE ( 'NONE', #9210, #4677 ) ;
#4516=ORIENTED_EDGE ( 'NONE', *, *, #294, .T. ) ;
#4628=CIRCLE ( 'NONE', #3963, 4.999999999999997335 ) ;
#4677=VECTOR ( 'NONE', #135, 1000.000000000000000 ) ;
#4725=CARTESIAN_POINT ( 'NONE',  ( 40.00000000000001421, 0.000000000000000000, 0.000000000000000000 ) ) ;
#4764=ORIENTED_EDGE ( 'NONE', *, *, #13776, .F. ) ;
#4784=CARTESIAN_POINT ( 'NONE',  ( 0.000000000000000000, -5.000000000000000888, -150.0000000000000000 ) ) ;
#4918=VERTEX_POINT ( 'NONE', #9309 ) ;
#4919=CARTESIAN_POINT ( 'NONE',  ( 0.000000000000000000, 0.000000000000000000, -150.0000000000000000 ) ) ;
#5004=CARTESIAN_POINT ( 'NONE',  ( 0.000000000000000000, -3.000000000000000888, 0.000000000000000000 ) ) ;
#5042=CARTESIAN_POINT ( 'NONE',  ( 0.000000000000000000, 0.000000000000000000, 0.000000000000000000 ) ) ;
#5069=DIRECTION ( 'NONE',  ( 1.000000000000000000, 0.000000000000000000, 0.000000000000000000 ) ) ;
#5099=AXIS2_PLACEMENT_3D ( 'NONE', #3509, #16101, #10112 ) ;
#5165=VERTEX_POINT ( 'NONE', #19993 ) ;
#5174=ADVANCED_FACE ( 'NONE', ( #5900 ), #10631, .T. ) ;
#5179=DIRECTION ( 'NONE',  ( 0.000000000000000000, -0.000000000000000000, 1.000000000000000000 ) ) ;
#5194=PRESENTATION_STYLE_ASSIGNMENT (( #229 ) ) ;
#5196=DIRECTION ( 'NONE',  ( -0.000000000000000000, -0.000000000000000000, 1.000000000000000000 ) ) ;
#5395=DIRECTION ( 'NONE',  ( -0.000000000000000000, -0.000000000000000000, 1.000000000000000000 ) ) ;
#5482=ORIENTED_EDGE ( 'NONE', *, *, #15181, .T. ) ;
#5501=LINE ( 'NONE', #15961, #13950 ) ;
#5628=DIRECTION ( 'NONE',  ( 1.000000000000000000, 0.000000000000000000, 0.000000000000000000 ) ) ;
#5638=ADVANCED_FACE ( 'NONE', ( #13363, #10237 ), #13541, .F. ) ;
#5715=SHAPE_DEFINITION_REPRESENTATION ( #10731, #13798 ) ;
#5749=CARTESIAN_POINT ( 'NONE',  ( 40.00000000000001421, 3.000000000000000888, 0.000000000000000000 ) ) ;
#5782=CARTESIAN_POINT ( 'NONE',  ( 40.00000000000001421, 3.000000000000000888, -150.0000000000000000 ) ) ;
#5900=FACE_OUTER_BOUND ( 'NONE', #2728, .T. ) ;
#6067=CARTESIAN_POINT ( 'NONE',  ( 40.00000000000001421, -3.000000000000000888, 0.000000000000000000 ) ) ;
#6093=ORIENTED_EDGE ( 'NONE', *, *, #8129, .F. ) ;
#6114=VERTEX_POINT ( 'NONE', #12920 ) ;
#6135=CARTESIAN_POINT ( 'NONE',  ( 40.00000000000001421, 0.000000000000000000, -150.0000000000000000 ) ) ;
#6186=DIRECTION ( 'NONE',  ( 1.000000000000000000, 0.000000000000000000, 0.000000000000000000 ) ) ;
#6222=LINE ( 'NONE', #9300, #6393 ) ;
#6286=LINE ( 'NONE', #18642, #10873 ) ;
#6309=FACE_OUTER_BOUND ( 'NONE', #3510, .T. ) ;
#6378=CLOSED_SHELL ( 'NONE', ( #18410, #14702, #5174, #18421, #19697, #11145, #5638, #11613, #8886, #3073, #12528, #9749 ) ) ;
#6393=VECTOR ( 'NONE', #20112, 1000.000000000000000 ) ;
#6417=ORIENTED_EDGE ( 'NONE', *, *, #655, .T. ) ;
#6432=DIRECTION ( 'NONE',  ( -0.000000000000000000, -0.000000000000000000, 1.000000000000000000 ) ) ;
#6457=CARTESIAN_POINT ( 'NONE',  ( 0.000000000000000000, -5.000000000000000888, 0.000000000000000000 ) ) ;
#6488=DIRECTION ( 'NONE',  ( -1.000000000000000000, 0.000000000000000000, 0.000000000000000000 ) ) ;
#6619=CARTESIAN_POINT ( 'NONE',  ( 40.00000000000001421, 0.000000000000000000, -150.0000000000000000 ) ) ;
#6656=DIRECTION ( 'NONE',  ( -0.000000000000000000, -0.000000000000000000, 1.000000000000000000 ) ) ;
#6674=CARTESIAN_POINT ( 'NONE',  ( 0.000000000000000000, -5.000000000000000888, -150.0000000000000000 ) ) ;
#6741=ORIENTED_EDGE ( 'NONE', *, *, #294, .F. ) ;
#6791=EDGE_LOOP ( 'NONE', ( #16556, #16142, #2018, #12518, #17552 ) ) ;
#6804=CARTESIAN_POINT ( 'NONE',  ( 40.00000000000001421, 3.000000000000000888, -150.0000000000000000 ) ) ;
#6840=CARTESIAN_POINT ( 'NONE',  ( 40.00000000000001421, -5.000000000000000888, -150.0000000000000000 ) ) ;
#6850=CARTESIAN_POINT ( 'NONE',  ( 40.00000000000001421, 3.000000000000000888, -150.0000000000000000 ) ) ;
#6898=DIRECTION ( 'NONE',  ( 0.000000000000000000, -0.000000000000000000, 1.000000000000000000 ) ) ;
#6933=ORIENTED_EDGE ( 'NONE', *, *, #7388, .T. ) ;
#6997=EDGE_CURVE ( 'NONE', #7067, #12183, #3250, .T. ) ;
#7038=AXIS2_PLACEMENT_3D ( 'NONE', #20143, #13770, #20259 ) ;
#7061=VERTEX_POINT ( 'NONE', #13303 ) ;
#7067=VERTEX_POINT ( 'NONE', #3819 ) ;
#7079=EDGE_CURVE ( 'NONE', #20011, #19900, #4628, .T. ) ;
#7137=ORIENTED_EDGE ( 'NONE', *, *, #12163, .T. ) ;
#7198=DIRECTION ( 'NONE',  ( -0.000000000000000000, -0.000000000000000000, 1.000000000000000000 ) ) ;
#7307=DIRECTION ( 'NONE',  ( 1.000000000000000000, 0.000000000000000000, 0.000000000000000000 ) ) ;
#7322=VERTEX_POINT ( 'NONE', #17525 ) ;
#7363=DIRECTION ( 'NONE',  ( 0.000000000000000000, 0.000000000000000000, 1.000000000000000000 ) ) ;
#7388=EDGE_CURVE ( 'NONE', #16045, #12183, #3734, .T. ) ;
#7441=ORIENTED_EDGE ( 'NONE', *, *, #1780, .T. ) ;
#7445=DIRECTION ( 'NONE',  ( 1.000000000000000000, 0.000000000000000000, 0.000000000000000000 ) ) ;
#7679=CARTESIAN_POINT ( 'NONE',  ( 0.000000000000000000, 0.000000000000000000, -150.0000000000000000 ) ) ;
#7726=LINE ( 'NONE', #18941, #16510 ) ;
#7752=AXIS2_PLACEMENT_3D ( 'NONE', #9111, #7363, #15400 ) ;
#7842=FACE_BOUND ( 'NONE', #19228, .T. ) ;
#7863=DIRECTION ( 'NONE',  ( 0.000000000000000000, -0.000000000000000000, -1.000000000000000000 ) ) ;
#7950=CIRCLE ( 'NONE', #2691, 3.000000000000000888 ) ;
#8023=CARTESIAN_POINT ( 'NONE',  ( 40.00000000000001421, 5.000000000000000888, -150.0000000000000000 ) ) ;
#8057=VECTOR ( 'NONE', #15621, 1000.000000000000000 ) ;
#8129=EDGE_CURVE ( 'NONE', #6114, #7322, #13572, .T. ) ;
#8141=DIRECTION ( 'NONE',  ( 1.000000000000000000, 0.000000000000000000, 0.000000000000000000 ) ) ;
#8227=EDGE_CURVE ( 'NONE', #7322, #8551, #2734, .T. ) ;
#8234=DIRECTION ( 'NONE',  ( 1.000000000000000000, 0.000000000000000000, 0.000000000000000000 ) ) ;
#8295=CARTESIAN_POINT ( 'NONE',  ( 40.00000000000001421, -3.000000000000000888, -150.0000000000000000 ) ) ;
#8322=ORIENTED_EDGE ( 'NONE', *, *, #9146, .T. ) ;
#8380=( NAMED_UNIT ( * ) SI_UNIT ( $, .STERADIAN. ) SOLID_ANGLE_UNIT ( ) );
#8551=VERTEX_POINT ( 'NONE', #2953 ) ;
#8578=EDGE_CURVE ( 'NONE', #10797, #4918, #7950, .T. ) ;
#8691=MECHANICAL_DESIGN_GEOMETRIC_PRESENTATION_REPRESENTATION('',(#3425),#1423);
#8734=CIRCLE ( 'NONE', #16004, 3.000000000000002665 ) ;
#8737=CARTESIAN_POINT ( 'NONE',  ( 0.000000000000000000, 3.000000000000000888, 0.000000000000000000 ) ) ;
#8764=VECTOR ( 'NONE', #6656, 1000.000000000000000 ) ;
#8824=AXIS2_PLACEMENT_3D ( 'NONE', #4784, #18774, #7863 ) ;
#8886=ADVANCED_FACE ( 'NONE', ( #9124 ), #1347, .F. ) ;
#8918=CARTESIAN_POINT ( 'NONE',  ( 0.000000000000000000, -3.000000000000000888, -150.0000000000000000 ) ) ;
#8939=DIRECTION ( 'NONE',  ( 0.000000000000000000, 0.000000000000000000, 1.000000000000000000 ) ) ;
#9097=DIRECTION ( 'NONE',  ( 0.000000000000000000, 0.000000000000000000, 1.000000000000000000 ) ) ;
#9111=CARTESIAN_POINT ( 'NONE',  ( 40.00000000000001421, 0.000000000000000000, -150.0000000000000000 ) ) ;
#9124=FACE_OUTER_BOUND ( 'NONE', #13351, .T. ) ;
#9146=EDGE_CURVE ( 'NONE', #6114, #9635, #4243, .T. ) ;
#9168=EDGE_LOOP ( 'NONE', ( #13093, #6093, #8322, #16697 ) ) ;
#9210=CARTESIAN_POINT ( 'NONE',  ( 0.000000000000000000, 5.000000000000000888, -150.0000000000000000 ) ) ;
#9300=CARTESIAN_POINT ( 'NONE',  ( 45.00000000000001421, 0.000000000000000000, -150.0000000000000000 ) ) ;
#9309=CARTESIAN_POINT ( 'NONE',  ( 0.000000000000000000, -3.000000000000000888, -150.0000000000000000 ) ) ;
#9311=VECTOR ( 'NONE', #5196, 1000.000000000000000 ) ;
#9367=CARTESIAN_POINT ( 'NONE',  ( 40.00000000000001421, 0.000000000000000000, 0.000000000000000000 ) ) ;
#9414=CYLINDRICAL_SURFACE ( 'NONE', #1289, 4.999999999999997335 ) ;
#9575=PRODUCT ( 'Part15', 'Part15', '', ( #18475 ) ) ;
#9635=VERTEX_POINT ( 'NONE', #6067 ) ;
#9656=ORIENTED_EDGE ( 'NONE', *, *, #6997, .T. ) ;
#9749=ADVANCED_FACE ( 'NONE', ( #11299 ), #272, .F. ) ;
#9769=DIRECTION ( 'NONE',  ( 0.000000000000000000, -1.000000000000000000, 0.000000000000000000 ) ) ;
#9803=CYLINDRICAL_SURFACE ( 'NONE', #1057, 3.000000000000002665 ) ;
#9921=LINE ( 'NONE', #6850, #9311 ) ;
#9928=ORIENTED_EDGE ( 'NONE', *, *, #1358, .T. ) ;
#9932=EDGE_CURVE ( 'NONE', #4918, #10186, #12430, .T. ) ;
#10009=CIRCLE ( 'NONE', #14263, 4.999999999999997335 ) ;
#10058=DIRECTION ( 'NONE',  ( 1.000000000000000000, 0.000000000000000000, 0.000000000000000000 ) ) ;
#10111=EDGE_LOOP ( 'NONE', ( #14154, #14275, #11074, #6741, #14265 ) ) ;
#10112=DIRECTION ( 'NONE',  ( 1.000000000000000000, 0.000000000000000000, 0.000000000000000000 ) ) ;
#10156=ORIENTED_EDGE ( 'NONE', *, *, #13297, .T. ) ;
#10186=VERTEX_POINT ( 'NONE', #5004 ) ;
#10237=FACE_OUTER_BOUND ( 'NONE', #10111, .T. ) ;
#10301=CARTESIAN_POINT ( 'NONE',  ( 45.00000000000001421, 0.000000000000000000, 0.000000000000000000 ) ) ;
#10303=CARTESIAN_POINT ( 'NONE',  ( 0.000000000000000000, 0.000000000000000000, 0.000000000000000000 ) ) ;
#10305=CARTESIAN_POINT ( 'NONE',  ( 40.00000000000001421, -5.000000000000000888, -150.0000000000000000 ) ) ;
#10369=ORIENTED_EDGE ( 'NONE', *, *, #18391, .T. ) ;
#10421=ORIENTED_EDGE ( 'NONE', *, *, #18391, .F. ) ;
#10447=DIRECTION ( 'NONE',  ( 1.000000000000000000, 0.000000000000000000, -0.000000000000000000 ) ) ;
#10631=CYLINDRICAL_SURFACE ( 'NONE', #3918, 5.000000000000000888 ) ;
#10731=PRODUCT_DEFINITION_SHAPE ( 'NONE', 'NONE',  #1129 ) ;
#10797=VERTEX_POINT ( 'NONE', #16577 ) ;
#10873=VECTOR ( 'NONE', #2965, 1000.000000000000000 ) ;
#10899=ORIENTED_EDGE ( 'NONE', *, *, #2223, .T. ) ;
#10951=ORIENTED_EDGE ( 'NONE', *, *, #18093, .T. ) ;
#11016=DIRECTION ( 'NONE',  ( 0.000000000000000000, 0.000000000000000000, 1.000000000000000000 ) ) ;
#11052=VECTOR ( 'NONE', #6432, 1000.000000000000000 ) ;
#11074=ORIENTED_EDGE ( 'NONE', *, *, #1780, .F. ) ;
#11145=ADVANCED_FACE ( 'NONE', ( #16847 ), #13841, .T. ) ;
#11249=( LENGTH_UNIT ( ) NAMED_UNIT ( * ) SI_UNIT ( .MILLI., .METRE. ) );
#11265=ORIENTED_EDGE ( 'NONE', *, *, #15569, .F. ) ;
#11299=FACE_OUTER_BOUND ( 'NONE', #14353, .T. ) ;
#11382=EDGE_CURVE ( 'NONE', #18513, #7061, #18017, .T. ) ;
#11391=ORIENTED_EDGE ( 'NONE', *, *, #7079, .T. ) ;
#11423=PLANE ( 'NONE',  #1033 ) ;
#11613=ADVANCED_FACE ( 'NONE', ( #7842, #6309 ), #15895, .T. ) ;
#11744=UNCERTAINTY_MEASURE_WITH_UNIT (LENGTH_MEASURE( 1.000000000000000082E-05 ), #16169, 'distance_accuracy_value', 'NONE');
#11810=VERTEX_POINT ( 'NONE', #5782 ) ;
#11903=EDGE_CURVE ( 'NONE', #3197, #10186, #17793, .T. ) ;
#11947=ORIENTED_EDGE ( 'NONE', *, *, #11382, .T. ) ;
#11958=CIRCLE ( 'NONE', #7038, 3.000000000000002665 ) ;
#12026=ORIENTED_EDGE ( 'NONE', *, *, #6997, .F. ) ;
#12081=DIRECTION ( 'NONE',  ( 0.000000000000000000, 0.000000000000000000, 1.000000000000000000 ) ) ;
#12163=EDGE_CURVE ( 'NONE', #12183, #20011, #10009, .T. ) ;
#12183=VERTEX_POINT ( 'NONE', #19020 ) ;
#12370=APPLICATION_CONTEXT ( 'automotive_design' ) ;
#12415=CARTESIAN_POINT ( 'NONE',  ( 40.00000000000001421, 5.000000000000000888, -150.0000000000000000 ) ) ;
#12430=LINE ( 'NONE', #8918, #17988 ) ;
#12486=CARTESIAN_POINT ( 'NONE',  ( 0.000000000000000000, -3.000000000000000888, 0.000000000000000000 ) ) ;
#12518=ORIENTED_EDGE ( 'NONE', *, *, #8129, .T. ) ;
#12528=ADVANCED_FACE ( 'NONE', ( #157 ), #1798, .F. ) ;
#12601=DIRECTION ( 'NONE',  ( 0.000000000000000000, 0.000000000000000000, 1.000000000000000000 ) ) ;
#12755=DIRECTION ( 'NONE',  ( 1.000000000000000000, 0.000000000000000000, 0.000000000000000000 ) ) ;
#12764=DIRECTION ( 'NONE',  ( 1.000000000000000000, 0.000000000000000000, 0.000000000000000000 ) ) ;
#12801=CARTESIAN_POINT ( 'NONE',  ( 0.000000000000000000, 0.000000000000000000, 0.000000000000000000 ) ) ;
#12835=EDGE_CURVE ( 'NONE', #4170, #19900, #2712, .T. ) ;
#12876=FACE_OUTER_BOUND ( 'NONE', #3136, .T. ) ;
#12908=CARTESIAN_POINT ( 'NONE',  ( 0.000000000000000000, 5.000000000000000888, -150.0000000000000000 ) ) ;
#12920=CARTESIAN_POINT ( 'NONE',  ( 40.00000000000001421, -3.000000000000000888, -150.0000000000000000 ) ) ;
#12923=SURFACE_STYLE_FILL_AREA ( #17648 ) ;
#12968=ORIENTED_EDGE ( 'NONE', *, *, #9932, .T. ) ;
#13093=ORIENTED_EDGE ( 'NONE', *, *, #8227, .F. ) ;
#13094=EDGE_CURVE ( 'NONE', #9635, #8551, #8734, .T. ) ;
#13197=VECTOR ( 'NONE', #3352, 1000.000000000000000 ) ;
#13295=VECTOR ( 'NONE', #17415, 1000.000000000000000 ) ;
#13297=EDGE_CURVE ( 'NONE', #8551, #5165, #2697, .T. ) ;
#13303=CARTESIAN_POINT ( 'NONE',  ( 0.000000000000000000, -5.000000000000000888, -150.0000000000000000 ) ) ;
#13320=ADVANCED_BREP_SHAPE_REPRESENTATION ( '', ( #1489, #2741 ), #13578 ) ;
#13340=VECTOR ( 'NONE', #12601, 1000.000000000000000 ) ;
#13343=CARTESIAN_POINT ( 'NONE',  ( 40.00000000000001421, 5.000000000000000888, 0.000000000000000000 ) ) ;
#13351=EDGE_LOOP ( 'NONE', ( #1975, #15977, #16047, #10899 ) ) ;
#13363=FACE_BOUND ( 'NONE', #6791, .T. ) ;
#13432=APPLICATION_CONTEXT ( 'automotive_design' ) ;
#13454=UNCERTAINTY_MEASURE_WITH_UNIT (LENGTH_MEASURE( 1.000000000000000082E-05 ), #11249, 'distance_accuracy_value', 'NONE');
#13485=FACE_OUTER_BOUND ( 'NONE', #17776, .T. ) ;
#13541=PLANE ( 'NONE',  #17094 ) ;
#13572=CIRCLE ( 'NONE', #16536, 3.000000000000002665 ) ;
#13578=( GEOMETRIC_REPRESENTATION_CONTEXT ( 3 ) GLOBAL_UNCERTAINTY_ASSIGNED_CONTEXT ( ( #11744 ) ) GLOBAL_UNIT_ASSIGNED_CONTEXT ( ( #16169, #2205, #2304 ) ) REPRESENTATION_CONTEXT ( 'NONE', 'WORKASPACE' ) );
#13619=CIRCLE ( 'NONE', #14603, 4.999999999999997335 ) ;
#13623=CARTESIAN_POINT ( 'NONE',  ( 40.00000000000001421, 0.000000000000000000, 0.000000000000000000 ) ) ;
#13770=DIRECTION ( 'NONE',  ( 0.000000000000000000, 0.000000000000000000, 1.000000000000000000 ) ) ;
#13776=EDGE_CURVE ( 'NONE', #11810, #5165, #9921, .T. ) ;
#13798=SHAPE_REPRESENTATION ( 'Part15', ( #2741 ), #13578 ) ;
#13841=PLANE ( 'NONE',  #8824 ) ;
#13950=VECTOR ( 'NONE', #18144, 1000.000000000000000 ) ;
#14122=DIRECTION ( 'NONE',  ( 0.000000000000000000, 0.000000000000000000, 1.000000000000000000 ) ) ;
#14134=ORIENTED_EDGE ( 'NONE', *, *, #17852, .T. ) ;
#14154=ORIENTED_EDGE ( 'NONE', *, *, #11382, .F. ) ;
#14186=EDGE_LOOP ( 'NONE', ( #2726, #15804, #10156, #4764 ) ) ;
#14192=ORIENTED_EDGE ( 'NONE', *, *, #16329, .F. ) ;
#14245=CARTESIAN_POINT ( 'NONE',  ( 0.000000000000000000, -5.000000000000000888, -150.0000000000000000 ) ) ;
#14263=AXIS2_PLACEMENT_3D ( 'NONE', #4725, #11016, #6186 ) ;
#14265=ORIENTED_EDGE ( 'NONE', *, *, #18731, .F. ) ;
#14275=ORIENTED_EDGE ( 'NONE', *, *, #17852, .F. ) ;
#14353=EDGE_LOOP ( 'NONE', ( #10369, #18052, #18944, #12968 ) ) ;
#14571=AXIS2_PLACEMENT_3D ( 'NONE', #12801, #14122, #1429 ) ;
#14603=AXIS2_PLACEMENT_3D ( 'NONE', #1419, #12081, #7445 ) ;
#14702=ADVANCED_FACE ( 'NONE', ( #2813 ), #1331, .T. ) ;
#14710=ORIENTED_EDGE ( 'NONE', *, *, #7388, .F. ) ;
#14712=DIRECTION ( 'NONE',  ( 0.000000000000000000, 0.000000000000000000, 1.000000000000000000 ) ) ;
#14757=DIRECTION ( 'NONE',  ( 1.000000000000000000, 0.000000000000000000, 0.000000000000000000 ) ) ;
#14939=DIRECTION ( 'NONE',  ( 0.000000000000000000, 0.000000000000000000, 1.000000000000000000 ) ) ;
#15036=PRODUCT_DEFINITION_CONTEXT ( 'detailed design', #13432, 'design' ) ;
#15181=EDGE_CURVE ( 'NONE', #7061, #7067, #1646, .T. ) ;
#15304=CIRCLE ( 'NONE', #5099, 4.999999999999997335 ) ;
#15400=DIRECTION ( 'NONE',  ( 1.000000000000000000, 0.000000000000000000, 0.000000000000000000 ) ) ;
#15526=AXIS2_PLACEMENT_3D ( 'NONE', #10303, #902, #2471 ) ;
#15569=EDGE_CURVE ( 'NONE', #18513, #3196, #5501, .T. ) ;
#15604=ORIENTED_EDGE ( 'NONE', *, *, #12835, .T. ) ;
#15621=DIRECTION ( 'NONE',  ( 0.000000000000000000, 0.000000000000000000, 1.000000000000000000 ) ) ;
#15630=ORIENTED_EDGE ( 'NONE', *, *, #11903, .F. ) ;
#15804=ORIENTED_EDGE ( 'NONE', *, *, #8227, .T. ) ;
#15807=CARTESIAN_POINT ( 'NONE',  ( 0.000000000000000000, 3.000000000000000888, -150.0000000000000000 ) ) ;
#15895=PLANE ( 'NONE',  #14571 ) ;
#15961=CARTESIAN_POINT ( 'NONE',  ( 0.000000000000000000, 5.000000000000000888, -150.0000000000000000 ) ) ;
#15977=ORIENTED_EDGE ( 'NONE', *, *, #9932, .F. ) ;
#16004=AXIS2_PLACEMENT_3D ( 'NONE', #13623, #5395, #2380 ) ;
#16045=VERTEX_POINT ( 'NONE', #10305 ) ;
#16047=ORIENTED_EDGE ( 'NONE', *, *, #8578, .F. ) ;
#16072=EDGE_LOOP ( 'NONE', ( #4516, #9928, #16396, #14710 ) ) ;
#16078=DIRECTION ( 'NONE',  ( 0.000000000000000000, -0.000000000000000000, -1.000000000000000000 ) ) ;
#16100=ORIENTED_EDGE ( 'NONE', *, *, #18731, .T. ) ;
#16101=DIRECTION ( 'NONE',  ( 0.000000000000000000, 0.000000000000000000, 1.000000000000000000 ) ) ;
#16142=ORIENTED_EDGE ( 'NONE', *, *, #8578, .T. ) ;
#16157=VECTOR ( 'NONE', #1072, 1000.000000000000000 ) ;
#16169=( LENGTH_UNIT ( ) NAMED_UNIT ( * ) SI_UNIT ( .MILLI., .METRE. ) );
#16190=DIRECTION ( 'NONE',  ( 1.000000000000000000, 0.000000000000000000, 0.000000000000000000 ) ) ;
#16213=PLANE ( 'NONE',  #19500 ) ;
#16228=LINE ( 'NONE', #15807, #11052 ) ;
#16229=FILL_AREA_STYLE_COLOUR ( '', #114 ) ;
#16243=AXIS2_PLACEMENT_3D ( 'NONE', #9367, #1830, #8141 ) ;
#16244=VECTOR ( 'NONE', #965, 1000.000000000000000 ) ;
#16261=DIRECTION ( 'NONE',  ( -0.000000000000000000, -0.000000000000000000, 1.000000000000000000 ) ) ;
#16329=EDGE_CURVE ( 'NONE', #19900, #3196, #2748, .T. ) ;
#16396=ORIENTED_EDGE ( 'NONE', *, *, #12163, .F. ) ;
#16404=DIRECTION ( 'NONE',  ( 1.000000000000000000, 0.000000000000000000, 0.000000000000000000 ) ) ;
#16428=DIRECTION ( 'NONE',  ( 0.000000000000000000, 0.000000000000000000, 1.000000000000000000 ) ) ;
#16440=ORIENTED_EDGE ( 'NONE', *, *, #12835, .F. ) ;
#16497=VECTOR ( 'NONE', #19288, 1000.000000000000000 ) ;
#16510=VECTOR ( 'NONE', #6488, 1000.000000000000000 ) ;
#16527=CARTESIAN_POINT ( 'NONE',  ( 0.000000000000000000, 0.000000000000000000, -150.0000000000000000 ) ) ;
#16536=AXIS2_PLACEMENT_3D ( 'NONE', #371, #14712, #3491 ) ;
#16556=ORIENTED_EDGE ( 'NONE', *, *, #17198, .T. ) ;
#16577=CARTESIAN_POINT ( 'NONE',  ( 0.000000000000000000, 3.000000000000000888, -150.0000000000000000 ) ) ;
#16697=ORIENTED_EDGE ( 'NONE', *, *, #13094, .T. ) ;
#16709=EDGE_CURVE ( 'NONE', #4918, #6114, #6286, .T. ) ;
#16764=ORIENTED_EDGE ( 'NONE', *, *, #2223, .F. ) ;
#16847=FACE_OUTER_BOUND ( 'NONE', #4029, .T. ) ;
#16936=CIRCLE ( 'NONE', #19227, 5.000000000000000888 ) ;
#17079=ORIENTED_EDGE ( 'NONE', *, *, #655, .F. ) ;
#17094=AXIS2_PLACEMENT_3D ( 'NONE', #18059, #19797, #10447 ) ;
#17156=CARTESIAN_POINT ( 'NONE',  ( 45.00000000000001421, 0.000000000000000000, -150.0000000000000000 ) ) ;
#17198=EDGE_CURVE ( 'NONE', #11810, #10797, #7726, .T. ) ;
#17246=EDGE_LOOP ( 'NONE', ( #4433, #7441, #15604, #500 ) ) ;
#17415=DIRECTION ( 'NONE',  ( 1.000000000000000000, 0.000000000000000000, 0.000000000000000000 ) ) ;
#17511=FACE_OUTER_BOUND ( 'NONE', #14186, .T. ) ;
#17525=CARTESIAN_POINT ( 'NONE',  ( 43.00000000000001421, 0.000000000000000000, -150.0000000000000000 ) ) ;
#17552=ORIENTED_EDGE ( 'NONE', *, *, #18467, .T. ) ;
#17648=FILL_AREA_STYLE ('',( #16229 ) ) ;
#17776=EDGE_LOOP ( 'NONE', ( #14192, #16440, #14134, #830 ) ) ;
#17793=CIRCLE ( 'NONE', #15526, 3.000000000000000888 ) ;
#17825=DIRECTION ( 'NONE',  ( 0.000000000000000000, 1.000000000000000000, 0.000000000000000000 ) ) ;
#17852=EDGE_CURVE ( 'NONE', #4170, #18513, #4485, .T. ) ;
#17988=VECTOR ( 'NONE', #18385, 1000.000000000000000 ) ;
#18017=CIRCLE ( 'NONE', #249, 5.000000000000000888 ) ;
#18052=ORIENTED_EDGE ( 'NONE', *, *, #9146, .F. ) ;
#18059=CARTESIAN_POINT ( 'NONE',  ( 0.000000000000000000, 0.000000000000000000, -150.0000000000000000 ) ) ;
#18093=EDGE_CURVE ( 'NONE', #5165, #3197, #18498, .T. ) ;
#18144=DIRECTION ( 'NONE',  ( 0.000000000000000000, 0.000000000000000000, 1.000000000000000000 ) ) ;
#18385=DIRECTION ( 'NONE',  ( -0.000000000000000000, -0.000000000000000000, 1.000000000000000000 ) ) ;
#18387=DIRECTION ( 'NONE',  ( -0.000000000000000000, -0.000000000000000000, 1.000000000000000000 ) ) ;
#18391=EDGE_CURVE ( 'NONE', #10186, #9635, #1628, .T. ) ;
#18408=ORIENTED_EDGE ( 'NONE', *, *, #15181, .F. ) ;
#18410=ADVANCED_FACE ( 'NONE', ( #17511 ), #9803, .F. ) ;
#18421=ADVANCED_FACE ( 'NONE', ( #13485 ), #16213, .T. ) ;
#18467=EDGE_CURVE ( 'NONE', #7322, #11810, #11958, .T. ) ;
#18475=PRODUCT_CONTEXT ( 'NONE', #12370, 'mechanical' ) ;
#18490=CARTESIAN_POINT ( 'NONE',  ( 43.00000000000001421, 0.000000000000000000, -150.0000000000000000 ) ) ;
#18498=LINE ( 'NONE', #5749, #16244 ) ;
#18513=VERTEX_POINT ( 'NONE', #2639 ) ;
#18642=CARTESIAN_POINT ( 'NONE',  ( 0.000000000000000000, -3.000000000000000888, -150.0000000000000000 ) ) ;
#18680=DIRECTION ( 'NONE',  ( 0.000000000000000000, 0.000000000000000000, 1.000000000000000000 ) ) ;
#18731=EDGE_CURVE ( 'NONE', #7061, #16045, #55, .T. ) ;
#18774=DIRECTION ( 'NONE',  ( 0.000000000000000000, -1.000000000000000000, 0.000000000000000000 ) ) ;
#18853=ORIENTED_EDGE ( 'NONE', *, *, #16329, .T. ) ;
#18875=DIRECTION ( 'NONE',  ( 1.000000000000000000, 0.000000000000000000, 0.000000000000000000 ) ) ;
#18941=CARTESIAN_POINT ( 'NONE',  ( 40.00000000000001421, 3.000000000000000888, -150.0000000000000000 ) ) ;
#18944=ORIENTED_EDGE ( 'NONE', *, *, #16709, .F. ) ;
#19020=CARTESIAN_POINT ( 'NONE',  ( 40.00000000000001421, -5.000000000000000888, 0.000000000000000000 ) ) ;
#19227=AXIS2_PLACEMENT_3D ( 'NONE', #19955, #8939, #7307 ) ;
#19228=EDGE_LOOP ( 'NONE', ( #15630, #19622, #1704, #19812, #10421 ) ) ;
#19288=DIRECTION ( 'NONE',  ( 0.000000000000000000, 0.000000000000000000, 1.000000000000000000 ) ) ;
#19500=AXIS2_PLACEMENT_3D ( 'NONE', #12908, #17825, #5179 ) ;
#19622=ORIENTED_EDGE ( 'NONE', *, *, #18093, .F. ) ;
#19697=ADVANCED_FACE ( 'NONE', ( #1651 ), #9414, .T. ) ;
#19715=DIRECTION ( 'NONE',  ( -0.000000000000000000, -0.000000000000000000, 1.000000000000000000 ) ) ;
#19797=DIRECTION ( 'NONE',  ( 0.000000000000000000, 0.000000000000000000, 1.000000000000000000 ) ) ;
#19812=ORIENTED_EDGE ( 'NONE', *, *, #13094, .F. ) ;
#19816=PRODUCT_DEFINITION_FORMATION_WITH_SPECIFIED_SOURCE ( 'ANY', '', #9575, .NOT_KNOWN. ) ;
#19900=VERTEX_POINT ( 'NONE', #13343 ) ;
#19955=CARTESIAN_POINT ( 'NONE',  ( 0.000000000000000000, 0.000000000000000000, 0.000000000000000000 ) ) ;
#19993=CARTESIAN_POINT ( 'NONE',  ( 40.00000000000001421, 3.000000000000000888, 0.000000000000000000 ) ) ;
#20011=VERTEX_POINT ( 'NONE', #10301 ) ;
#20112=DIRECTION ( 'NONE',  ( 0.000000000000000000, 0.000000000000000000, 1.000000000000000000 ) ) ;
#20143=CARTESIAN_POINT ( 'NONE',  ( 40.00000000000001421, 0.000000000000000000, -150.0000000000000000 ) ) ;
#20259=DIRECTION ( 'NONE',  ( 1.000000000000000000, 0.000000000000000000, 0.000000000000000000 ) ) ;
ENDSEC;
END-ISO-10303-21;
